ISO-10303-21;
HEADER;
/* Generated by software containing ST-Developer
 * from STEP Tools, Inc. (www.steptools.com) 
 */

FILE_DESCRIPTION(
/* description */ ('Hand wheel with handle and shaft collar'),
/* implementation_level */ '2;1');

FILE_NAME(
/* name */ 'Seals 2RS (1).step',
/* time_stamp */ '2026-10-28T03:23:19-07:00',
/* author */ (''),
/* organization */ (''),
/* preprocessor_version */ 'ST-DEVELOPER v20.2',
/* originating_system */ 'Autodesk Translation Framework v15.17.0.0',
/* authorisation */ '');

FILE_SCHEMA (('AUTOMOTIVE_DESIGN { 1 0 10303 214 3 1 1 }'));
ENDSEC;

DATA;
#10=MECHANICAL_DESIGN_GEOMETRIC_PRESENTATION_REPRESENTATION('',(#437,#438),#10510);
#359=SHAPE_REPRESENTATION_RELATIONSHIP('SRR','None',#10678,#391);
#391=ADVANCED_BREP_SHAPE_REPRESENTATION('',(#482,#483),#10505);
#437=STYLED_ITEM('',(#10908),#482);
#438=STYLED_ITEM('',(#10908),#483);
#482=MANIFOLD_SOLID_BREP('Body1',#5338);
#483=MANIFOLD_SOLID_BREP('Body2',#5339);
#588=FACE_BOUND('',#1469,.T.);
#589=FACE_BOUND('',#1472,.T.);
#590=FACE_BOUND('',#1475,.T.);
#591=FACE_BOUND('',#1478,.T.);
#743=PLANE('',#6305);
#744=PLANE('',#6310);
#745=PLANE('',#6313);
#746=PLANE('',#6318);
#1047=FACE_OUTER_BOUND('',#1468,.T.);
#1048=FACE_OUTER_BOUND('',#1470,.T.);
#1049=FACE_OUTER_BOUND('',#1471,.T.);
#1050=FACE_OUTER_BOUND('',#1473,.T.);
#1051=FACE_OUTER_BOUND('',#1474,.T.);
#1052=FACE_OUTER_BOUND('',#1476,.T.);
#1053=FACE_OUTER_BOUND('',#1477,.T.);
#1054=FACE_OUTER_BOUND('',#1479,.T.);
#1468=EDGE_LOOP('',(#4761));
#1469=EDGE_LOOP('',(#4762));
#1470=EDGE_LOOP('',(#4763,#4764,#4765,#4766));
#1471=EDGE_LOOP('',(#4767));
#1472=EDGE_LOOP('',(#4768));
#1473=EDGE_LOOP('',(#4769,#4770,#4771,#4772));
#1474=EDGE_LOOP('',(#4773));
#1475=EDGE_LOOP('',(#4774));
#1476=EDGE_LOOP('',(#4775,#4776,#4777,#4778));
#1477=EDGE_LOOP('',(#4779));
#1478=EDGE_LOOP('',(#4780));
#1479=EDGE_LOOP('',(#4781,#4782,#4783,#4784));
#1790=LINE('',#10256,#2100);
#1791=LINE('',#10261,#2101);
#1792=LINE('',#10270,#2102);
#1793=LINE('',#10275,#2103);
#2100=VECTOR('',#7922,1.013815);
#2101=VECTOR('',#7929,0.991185);
#2102=VECTOR('',#7940,1.013815);
#2103=VECTOR('',#7947,0.991185);
#2418=CIRCLE('',#6306,1.013815);
#2419=CIRCLE('',#6307,0.991185);
#2420=CIRCLE('',#6309,1.013815);
#2421=CIRCLE('',#6311,0.991185);
#2422=CIRCLE('',#6314,1.013815);
#2423=CIRCLE('',#6315,0.991185);
#2424=CIRCLE('',#6317,1.013815);
#2425=CIRCLE('',#6319,0.991185);
#2858=VERTEX_POINT('',#10249);
#2859=VERTEX_POINT('',#10251);
#2860=VERTEX_POINT('',#10254);
#2861=VERTEX_POINT('',#10258);
#2862=VERTEX_POINT('',#10263);
#2863=VERTEX_POINT('',#10265);
#2864=VERTEX_POINT('',#10268);
#2865=VERTEX_POINT('',#10272);
#3498=EDGE_CURVE('',#2858,#2858,#2418,.T.);
#3499=EDGE_CURVE('',#2859,#2859,#2419,.T.);
#3500=EDGE_CURVE('',#2860,#2860,#2420,.T.);
#3501=EDGE_CURVE('',#2860,#2858,#1790,.T.);
#3502=EDGE_CURVE('',#2861,#2861,#2421,.T.);
#3503=EDGE_CURVE('',#2861,#2859,#1791,.T.);
#3504=EDGE_CURVE('',#2862,#2862,#2422,.T.);
#3505=EDGE_CURVE('',#2863,#2863,#2423,.T.);
#3506=EDGE_CURVE('',#2864,#2864,#2424,.T.);
#3507=EDGE_CURVE('',#2864,#2862,#1792,.T.);
#3508=EDGE_CURVE('',#2865,#2865,#2425,.T.);
#3509=EDGE_CURVE('',#2865,#2863,#1793,.T.);
#4761=ORIENTED_EDGE('',*,*,#3498,.F.);
#4762=ORIENTED_EDGE('',*,*,#3499,.T.);
#4763=ORIENTED_EDGE('',*,*,#3500,.F.);
#4764=ORIENTED_EDGE('',*,*,#3501,.T.);
#4765=ORIENTED_EDGE('',*,*,#3498,.T.);
#4766=ORIENTED_EDGE('',*,*,#3501,.F.);
#4767=ORIENTED_EDGE('',*,*,#3500,.T.);
#4768=ORIENTED_EDGE('',*,*,#3502,.F.);
#4769=ORIENTED_EDGE('',*,*,#3502,.T.);
#4770=ORIENTED_EDGE('',*,*,#3503,.T.);
#4771=ORIENTED_EDGE('',*,*,#3499,.F.);
#4772=ORIENTED_EDGE('',*,*,#3503,.F.);
#4773=ORIENTED_EDGE('',*,*,#3504,.F.);
#4774=ORIENTED_EDGE('',*,*,#3505,.T.);
#4775=ORIENTED_EDGE('',*,*,#3506,.F.);
#4776=ORIENTED_EDGE('',*,*,#3507,.T.);
#4777=ORIENTED_EDGE('',*,*,#3504,.T.);
#4778=ORIENTED_EDGE('',*,*,#3507,.F.);
#4779=ORIENTED_EDGE('',*,*,#3506,.T.);
#4780=ORIENTED_EDGE('',*,*,#3508,.F.);
#4781=ORIENTED_EDGE('',*,*,#3508,.T.);
#4782=ORIENTED_EDGE('',*,*,#3509,.T.);
#4783=ORIENTED_EDGE('',*,*,#3505,.F.);
#4784=ORIENTED_EDGE('',*,*,#3509,.F.);
#4964=CYLINDRICAL_SURFACE('',#6308,1.013815);
#4965=CYLINDRICAL_SURFACE('',#6312,0.991185);
#4966=CYLINDRICAL_SURFACE('',#6316,1.013815);
#4967=CYLINDRICAL_SURFACE('',#6320,0.991185);
#5259=ADVANCED_FACE('',(#1047,#588),#743,.T.);
#5260=ADVANCED_FACE('',(#1048),#4964,.T.);
#5261=ADVANCED_FACE('',(#1049,#589),#744,.T.);
#5262=ADVANCED_FACE('',(#1050),#4965,.F.);
#5263=ADVANCED_FACE('',(#1051,#590),#745,.T.);
#5264=ADVANCED_FACE('',(#1052),#4966,.T.);
#5265=ADVANCED_FACE('',(#1053,#591),#746,.T.);
#5266=ADVANCED_FACE('',(#1054),#4967,.F.);
#5338=CLOSED_SHELL('',(#5259,#5260,#5261,#5262));
#5339=CLOSED_SHELL('',(#5263,#5264,#5265,#5266));
#6304=AXIS2_PLACEMENT_3D('',#10247,#7910,#7911);
#6305=AXIS2_PLACEMENT_3D('',#10248,#7912,#7913);
#6306=AXIS2_PLACEMENT_3D('',#10250,#7914,#7915);
#6307=AXIS2_PLACEMENT_3D('',#10252,#7916,#7917);
#6308=AXIS2_PLACEMENT_3D('',#10253,#7918,#7919);
#6309=AXIS2_PLACEMENT_3D('',#10255,#7920,#7921);
#6310=AXIS2_PLACEMENT_3D('',#10257,#7923,#7924);
#6311=AXIS2_PLACEMENT_3D('',#10259,#7925,#7926);
#6312=AXIS2_PLACEMENT_3D('',#10260,#7927,#7928);
#6313=AXIS2_PLACEMENT_3D('',#10262,#7930,#7931);
#6314=AXIS2_PLACEMENT_3D('',#10264,#7932,#7933);
#6315=AXIS2_PLACEMENT_3D('',#10266,#7934,#7935);
#6316=AXIS2_PLACEMENT_3D('',#10267,#7936,#7937);
#6317=AXIS2_PLACEMENT_3D('',#10269,#7938,#7939);
#6318=AXIS2_PLACEMENT_3D('',#10271,#7941,#7942);
#6319=AXIS2_PLACEMENT_3D('',#10273,#7943,#7944);
#6320=AXIS2_PLACEMENT_3D('',#10274,#7945,#7946);
#7910=DIRECTION('axis',(0.,0.,1.));
#7911=DIRECTION('refdir',(1.,0.,0.));
#7912=DIRECTION('center_axis',(0.,1.,0.));
#7913=DIRECTION('ref_axis',(0.,0.,1.));
#7914=DIRECTION('center_axis',(0.,-1.,0.));
#7915=DIRECTION('ref_axis',(1.,0.,0.));
#7916=DIRECTION('center_axis',(0.,-1.,0.));
#7917=DIRECTION('ref_axis',(1.,0.,0.));
#7918=DIRECTION('center_axis',(0.,-1.,0.));
#7919=DIRECTION('ref_axis',(1.,0.,0.));
#7920=DIRECTION('center_axis',(0.,-1.,0.));
#7921=DIRECTION('ref_axis',(1.,0.,0.));
#7922=DIRECTION('',(0.,1.,0.));
#7923=DIRECTION('center_axis',(0.,-1.,0.));
#7924=DIRECTION('ref_axis',(0.,0.,-1.));
#7925=DIRECTION('center_axis',(0.,-1.,0.));
#7926=DIRECTION('ref_axis',(1.,0.,0.));
#7927=DIRECTION('center_axis',(0.,-1.,0.));
#7928=DIRECTION('ref_axis',(1.,0.,0.));
#7929=DIRECTION('',(0.,1.,0.));
#7930=DIRECTION('center_axis',(0.,1.,0.));
#7931=DIRECTION('ref_axis',(0.,0.,1.));
#7932=DIRECTION('center_axis',(0.,-1.,0.));
#7933=DIRECTION('ref_axis',(1.,0.,0.));
#7934=DIRECTION('center_axis',(0.,-1.,0.));
#7935=DIRECTION('ref_axis',(1.,0.,0.));
#7936=DIRECTION('center_axis',(0.,-1.,0.));
#7937=DIRECTION('ref_axis',(1.,0.,0.));
#7938=DIRECTION('center_axis',(0.,-1.,0.));
#7939=DIRECTION('ref_axis',(1.,0.,0.));
#7940=DIRECTION('',(0.,1.,0.));
#7941=DIRECTION('center_axis',(0.,-1.,0.));
#7942=DIRECTION('ref_axis',(0.,0.,-1.));
#7943=DIRECTION('center_axis',(0.,-1.,0.));
#7944=DIRECTION('ref_axis',(1.,0.,0.));
#7945=DIRECTION('center_axis',(0.,-1.,0.));
#7946=DIRECTION('ref_axis',(1.,0.,0.));
#7947=DIRECTION('',(0.,1.,0.));
#10247=CARTESIAN_POINT('',(0.,0.,0.));
#10248=CARTESIAN_POINT('Origin',(1.013815,0.445,0.));
#10249=CARTESIAN_POINT('',(-1.013815,0.445,-1.24156529467757E-16));
#10250=CARTESIAN_POINT('Origin',(0.,0.445,0.));
#10251=CARTESIAN_POINT('',(-0.991185,0.445,-1.21385153761287E-16));
#10252=CARTESIAN_POINT('Origin',(0.,0.445,0.));
#10253=CARTESIAN_POINT('Origin',(0.,0.4075,0.));
#10254=CARTESIAN_POINT('',(-1.013815,0.37,-1.24156529467757E-16));
#10255=CARTESIAN_POINT('Origin',(0.,0.37,0.));
#10256=CARTESIAN_POINT('',(-1.013815,0.4075,-1.24156529467757E-16));
#10257=CARTESIAN_POINT('Origin',(0.991185,0.37,0.));
#10258=CARTESIAN_POINT('',(-0.991185,0.37,-1.21385153761287E-16));
#10259=CARTESIAN_POINT('Origin',(0.,0.37,0.));
#10260=CARTESIAN_POINT('Origin',(0.,0.4075,0.));
#10261=CARTESIAN_POINT('',(-0.991185,0.4075,-1.21385153761287E-16));
#10262=CARTESIAN_POINT('Origin',(1.013815,-0.37,0.));
#10263=CARTESIAN_POINT('',(-1.013815,-0.37,-1.24156529467757E-16));
#10264=CARTESIAN_POINT('Origin',(0.,-0.37,0.));
#10265=CARTESIAN_POINT('',(-0.991185,-0.37,-1.21385153761287E-16));
#10266=CARTESIAN_POINT('Origin',(0.,-0.37,0.));
#10267=CARTESIAN_POINT('Origin',(0.,-0.4075,0.));
#10268=CARTESIAN_POINT('',(-1.013815,-0.445,-1.24156529467757E-16));
#10269=CARTESIAN_POINT('Origin',(0.,-0.445,0.));
#10270=CARTESIAN_POINT('',(-1.013815,-0.4075,-1.24156529467757E-16));
#10271=CARTESIAN_POINT('Origin',(0.991185,-0.445,0.));
#10272=CARTESIAN_POINT('',(-0.991185,-0.445,-1.21385153761287E-16));
#10273=CARTESIAN_POINT('Origin',(0.,-0.445,0.));
#10274=CARTESIAN_POINT('Origin',(0.,-0.4075,0.));
#10275=CARTESIAN_POINT('',(-0.991185,-0.4075,-1.21385153761287E-16));
#10466=UNCERTAINTY_MEASURE_WITH_UNIT(LENGTH_MEASURE(0.001),#10511,
'DISTANCE_ACCURACY_VALUE',
'Maximum model space distance between geometric entities at asserted c
onnectivities');
#10471=UNCERTAINTY_MEASURE_WITH_UNIT(LENGTH_MEASURE(0.001),#10511,
'DISTANCE_ACCURACY_VALUE',
'Maximum model space distance between geometric entities at asserted c
onnectivities');
#10505=(
GEOMETRIC_REPRESENTATION_CONTEXT(3)
GLOBAL_UNCERTAINTY_ASSIGNED_CONTEXT((#10466))
GLOBAL_UNIT_ASSIGNED_CONTEXT((#10511,#10513,#10514))
REPRESENTATION_CONTEXT('','3D')
);
#10510=(
GEOMETRIC_REPRESENTATION_CONTEXT(3)
GLOBAL_UNCERTAINTY_ASSIGNED_CONTEXT((#10471))
GLOBAL_UNIT_ASSIGNED_CONTEXT((#10511,#10513,#10514))
REPRESENTATION_CONTEXT('','3D')
);
#10511=(
LENGTH_UNIT()
NAMED_UNIT(*)
SI_UNIT(.CENTI.,.METRE.)
);
#10513=(
NAMED_UNIT(*)
PLANE_ANGLE_UNIT()
SI_UNIT($,.RADIAN.)
);
#10514=(
NAMED_UNIT(*)
SI_UNIT($,.STERADIAN.)
SOLID_ANGLE_UNIT()
);
#10548=SHAPE_DEFINITION_REPRESENTATION(#10591,#10678);
#10591=PRODUCT_DEFINITION_SHAPE('',$,#10717);
#10678=SHAPE_REPRESENTATION('',(#6304),#10505);
#10683=PRODUCT_DEFINITION_CONTEXT('part definition',#10799,'design');
#10717=PRODUCT_DEFINITION('Seals 2RS (1)','Seals 2RS (1)',#10755,#10683);
#10755=PRODUCT_DEFINITION_FORMATION('',$,#10834);
#10799=APPLICATION_CONTEXT(
'Core Data for Automotive Mechanical Design Process');
#10800=PRODUCT_CONTEXT('part definition',#10799,'mechanical');
#10834=PRODUCT('Seals 2RS (1)','Seals 2RS (1)','Seals 2RS (1)',(#10800));
#10902=COLOUR_RGB('Grey',0.48,0.52,0.57);
#10903=FILL_AREA_STYLE_COLOUR('',#10902);
#10904=FILL_AREA_STYLE('',(#10903));
#10905=SURFACE_STYLE_FILL_AREA(#10904);
#10906=SURFACE_SIDE_STYLE('',(#10905));
#10907=SURFACE_STYLE_USAGE(.BOTH.,#10906);
#10908=PRESENTATION_STYLE_ASSIGNMENT((#10907));
ENDSEC;
END-ISO-10303-21;
